ISO-10303-21;
HEADER;
/* Generated by software containing ST-Developer
 * from STEP Tools, Inc. (www.steptools.com) 
 */

FILE_DESCRIPTION(
/* description */ ('Line shaft on three pillow blocks'),
/* implementation_level */ '2;1');

FILE_NAME(
/* name */ 'Flat Washer - M8.step',
/* time_stamp */ '2026-10-27T10:49:19-07:00',
/* author */ (''),
/* organization */ (''),
/* preprocessor_version */ 'ST-DEVELOPER v20.2',
/* originating_system */ 'Autodesk Translation Framework v15.17.0.0',
/* authorisation */ '');

FILE_SCHEMA (('AUTOMOTIVE_DESIGN { 1 0 10303 214 3 1 1 }'));
ENDSEC;

DATA;
#10=MECHANICAL_DESIGN_GEOMETRIC_PRESENTATION_REPRESENTATION('',(#354),#8377);
#299=SHAPE_REPRESENTATION_RELATIONSHIP('SRR','None',#8515,#326);
#326=ADVANCED_BREP_SHAPE_REPRESENTATION('',(#381),#8364);
#354=STYLED_ITEM('',(#8725),#381);
#381=MANIFOLD_SOLID_BREP('Body1',#4341);
#459=FACE_BOUND('',#1111,.T.);
#460=FACE_BOUND('',#1113,.T.);
#571=PLANE('',#4904);
#572=PLANE('',#4905);
#788=FACE_OUTER_BOUND('',#1108,.T.);
#789=FACE_OUTER_BOUND('',#1109,.T.);
#790=FACE_OUTER_BOUND('',#1110,.T.);
#791=FACE_OUTER_BOUND('',#1112,.T.);
#1108=EDGE_LOOP('',(#3513,#3514,#3515,#3516));
#1109=EDGE_LOOP('',(#3517,#3518,#3519,#3520));
#1110=EDGE_LOOP('',(#3521));
#1111=EDGE_LOOP('',(#3522));
#1112=EDGE_LOOP('',(#3523));
#1113=EDGE_LOOP('',(#3524));
#1423=LINE('',#7508,#1750);
#1424=LINE('',#7514,#1751);
#1750=VECTOR('',#5810,0.42);
#1751=VECTOR('',#5817,0.8);
#1999=CIRCLE('',#4899,0.42);
#2000=CIRCLE('',#4900,0.42);
#2001=CIRCLE('',#4902,0.8);
#2002=CIRCLE('',#4903,0.8);
#2262=VERTEX_POINT('',#7505);
#2263=VERTEX_POINT('',#7507);
#2264=VERTEX_POINT('',#7511);
#2265=VERTEX_POINT('',#7513);
#2705=EDGE_CURVE('',#2262,#2262,#1999,.T.);
#2706=EDGE_CURVE('',#2262,#2263,#1423,.T.);
#2707=EDGE_CURVE('',#2263,#2263,#2000,.T.);
#2708=EDGE_CURVE('',#2264,#2264,#2001,.T.);
#2709=EDGE_CURVE('',#2264,#2265,#1424,.T.);
#2710=EDGE_CURVE('',#2265,#2265,#2002,.T.);
#3513=ORIENTED_EDGE('',*,*,#2705,.F.);
#3514=ORIENTED_EDGE('',*,*,#2706,.T.);
#3515=ORIENTED_EDGE('',*,*,#2707,.T.);
#3516=ORIENTED_EDGE('',*,*,#2706,.F.);
#3517=ORIENTED_EDGE('',*,*,#2708,.F.);
#3518=ORIENTED_EDGE('',*,*,#2709,.T.);
#3519=ORIENTED_EDGE('',*,*,#2710,.T.);
#3520=ORIENTED_EDGE('',*,*,#2709,.F.);
#3521=ORIENTED_EDGE('',*,*,#2708,.T.);
#3522=ORIENTED_EDGE('',*,*,#2705,.T.);
#3523=ORIENTED_EDGE('',*,*,#2710,.F.);
#3524=ORIENTED_EDGE('',*,*,#2707,.F.);
#4046=CYLINDRICAL_SURFACE('',#4898,0.42);
#4047=CYLINDRICAL_SURFACE('',#4901,0.8);
#4206=ADVANCED_FACE('',(#788),#4046,.F.);
#4207=ADVANCED_FACE('',(#789),#4047,.T.);
#4208=ADVANCED_FACE('',(#790,#459),#571,.T.);
#4209=ADVANCED_FACE('',(#791,#460),#572,.F.);
#4341=CLOSED_SHELL('',(#4206,#4207,#4208,#4209));
#4897=AXIS2_PLACEMENT_3D('',#7503,#5804,#5805);
#4898=AXIS2_PLACEMENT_3D('',#7504,#5806,#5807);
#4899=AXIS2_PLACEMENT_3D('',#7506,#5808,#5809);
#4900=AXIS2_PLACEMENT_3D('',#7509,#5811,#5812);
#4901=AXIS2_PLACEMENT_3D('',#7510,#5813,#5814);
#4902=AXIS2_PLACEMENT_3D('',#7512,#5815,#5816);
#4903=AXIS2_PLACEMENT_3D('',#7515,#5818,#5819);
#4904=AXIS2_PLACEMENT_3D('',#7516,#5820,#5821);
#4905=AXIS2_PLACEMENT_3D('',#7517,#5822,#5823);
#5804=DIRECTION('axis',(0.,0.,1.));
#5805=DIRECTION('refdir',(1.,0.,0.));
#5806=DIRECTION('center_axis',(0.,1.,0.));
#5807=DIRECTION('ref_axis',(1.,0.,0.));
#5808=DIRECTION('center_axis',(0.,-1.,0.));
#5809=DIRECTION('ref_axis',(1.,0.,0.));
#5810=DIRECTION('',(0.,-1.,0.));
#5811=DIRECTION('center_axis',(0.,-1.,0.));
#5812=DIRECTION('ref_axis',(1.,0.,0.));
#5813=DIRECTION('center_axis',(0.,1.,0.));
#5814=DIRECTION('ref_axis',(1.,0.,0.));
#5815=DIRECTION('center_axis',(0.,1.,0.));
#5816=DIRECTION('ref_axis',(1.,0.,0.));
#5817=DIRECTION('',(0.,-1.,0.));
#5818=DIRECTION('center_axis',(0.,1.,0.));
#5819=DIRECTION('ref_axis',(1.,0.,0.));
#5820=DIRECTION('center_axis',(0.,1.,0.));
#5821=DIRECTION('ref_axis',(1.,0.,0.));
#5822=DIRECTION('center_axis',(0.,1.,0.));
#5823=DIRECTION('ref_axis',(1.,0.,0.));
#7503=CARTESIAN_POINT('',(0.,0.,0.));
#7504=CARTESIAN_POINT('Origin',(0.,0.,0.));
#7505=CARTESIAN_POINT('',(-0.42,0.16,5.14351655641888E-17));
#7506=CARTESIAN_POINT('Origin',(0.,0.16,0.));
#7507=CARTESIAN_POINT('',(-0.42,0.,5.14351655641888E-17));
#7508=CARTESIAN_POINT('',(-0.42,0.,5.14351655641888E-17));
#7509=CARTESIAN_POINT('Origin',(0.,0.,0.));
#7510=CARTESIAN_POINT('Origin',(0.,0.,0.));
#7511=CARTESIAN_POINT('',(-0.8,0.16,9.79717439317883E-17));
#7512=CARTESIAN_POINT('Origin',(0.,0.16,0.));
#7513=CARTESIAN_POINT('',(-0.8,0.,9.79717439317883E-17));
#7514=CARTESIAN_POINT('',(-0.8,0.,9.79717439317883E-17));
#7515=CARTESIAN_POINT('Origin',(0.,0.,0.));
#7516=CARTESIAN_POINT('Origin',(0.,0.16,0.));
#7517=CARTESIAN_POINT('Origin',(0.,0.,0.));
#8332=UNCERTAINTY_MEASURE_WITH_UNIT(LENGTH_MEASURE(0.001),#8378,
'DISTANCE_ACCURACY_VALUE',
'Maximum model space distance between geometric entities at asserted c
onnectivities');
#8345=UNCERTAINTY_MEASURE_WITH_UNIT(LENGTH_MEASURE(0.001),#8378,
'DISTANCE_ACCURACY_VALUE',
'Maximum model space distance between geometric entities at asserted c
onnectivities');
#8364=(
GEOMETRIC_REPRESENTATION_CONTEXT(3)
GLOBAL_UNCERTAINTY_ASSIGNED_CONTEXT((#8332))
GLOBAL_UNIT_ASSIGNED_CONTEXT((#8378,#8380,#8381))
REPRESENTATION_CONTEXT('','3D')
);
#8377=(
GEOMETRIC_REPRESENTATION_CONTEXT(3)
GLOBAL_UNCERTAINTY_ASSIGNED_CONTEXT((#8345))
GLOBAL_UNIT_ASSIGNED_CONTEXT((#8378,#8380,#8381))
REPRESENTATION_CONTEXT('','3D')
);
#8378=(
LENGTH_UNIT()
NAMED_UNIT(*)
SI_UNIT(.CENTI.,.METRE.)
);
#8380=(
NAMED_UNIT(*)
PLANE_ANGLE_UNIT()
SI_UNIT($,.RADIAN.)
);
#8381=(
NAMED_UNIT(*)
SI_UNIT($,.STERADIAN.)
SOLID_ANGLE_UNIT()
);
#8400=SHAPE_DEFINITION_REPRESENTATION(#8433,#8515);
#8433=PRODUCT_DEFINITION_SHAPE('',$,#8547);
#8515=SHAPE_REPRESENTATION('',(#4897),#8364);
#8528=PRODUCT_DEFINITION_CONTEXT('part definition',#8623,'design');
#8547=PRODUCT_DEFINITION('Flat Washer - M8','Flat Washer - M8',#8578,#8528);
#8578=PRODUCT_DEFINITION_FORMATION('',$,#8643);
#8623=APPLICATION_CONTEXT(
'Core Data for Automotive Mechanical Design Process');
#8624=PRODUCT_CONTEXT('part definition',#8623,'mechanical');
#8643=PRODUCT('Flat Washer - M8','Flat Washer - M8','Flat Washer - M8',
(#8624));
#8719=COLOUR_RGB('Black',0.12,0.14,0.17);
#8720=FILL_AREA_STYLE_COLOUR('',#8719);
#8721=FILL_AREA_STYLE('',(#8720));
#8722=SURFACE_STYLE_FILL_AREA(#8721);
#8723=SURFACE_SIDE_STYLE('',(#8722));
#8724=SURFACE_STYLE_USAGE(.BOTH.,#8723);
#8725=PRESENTATION_STYLE_ASSIGNMENT((#8724));
ENDSEC;
END-ISO-10303-21;
